ISO-10303-21;
HEADER;
/* Generated by software containing ST-Developer
 * from STEP Tools, Inc. (www.steptools.com) 
 */

FILE_DESCRIPTION(
/* description */ ('Bin tilter linkage'),
/* implementation_level */ '2;1');

FILE_NAME(
/* name */ 'Pivot keeper (2).step',
/* time_stamp */ '2026-10-28T03:26:24-07:00',
/* author */ (''),
/* organization */ (''),
/* preprocessor_version */ 'ST-DEVELOPER v20.2',
/* originating_system */ 'Autodesk Translation Framework v15.17.0.0',
/* authorisation */ '');

FILE_SCHEMA (('AUTOMOTIVE_DESIGN { 1 0 10303 214 3 1 1 }'));
ENDSEC;

DATA;
#10=MECHANICAL_DESIGN_GEOMETRIC_PRESENTATION_REPRESENTATION('',(#954),#23728);
#734=SHAPE_REPRESENTATION_RELATIONSHIP('SRR','None',#24202,#840);
#840=ADVANCED_BREP_SHAPE_REPRESENTATION('',(#1067),#23702);
#954=STYLED_ITEM('',(#24779),#1067);
#1067=MANIFOLD_SOLID_BREP('Body1',#12485);
#1426=FACE_BOUND('',#3625,.T.);
#1427=FACE_BOUND('',#3627,.T.);
#1792=PLANE('',#15073);
#1793=PLANE('',#15074);
#2506=FACE_OUTER_BOUND('',#3622,.T.);
#2507=FACE_OUTER_BOUND('',#3623,.T.);
#2508=FACE_OUTER_BOUND('',#3624,.T.);
#2509=FACE_OUTER_BOUND('',#3626,.T.);
#3622=EDGE_LOOP('',(#10675,#10676,#10677,#10678));
#3623=EDGE_LOOP('',(#10679,#10680,#10681,#10682));
#3624=EDGE_LOOP('',(#10683));
#3625=EDGE_LOOP('',(#10684));
#3626=EDGE_LOOP('',(#10685));
#3627=EDGE_LOOP('',(#10686));
#4353=LINE('',#22726,#5028);
#4354=LINE('',#22732,#5029);
#5028=VECTOR('',#18764,0.225);
#5029=VECTOR('',#18771,1.);
#5832=CIRCLE('',#15068,0.225);
#5833=CIRCLE('',#15069,0.225);
#5834=CIRCLE('',#15071,1.);
#5835=CIRCLE('',#15072,1.);
#6731=VERTEX_POINT('',#22723);
#6732=VERTEX_POINT('',#22725);
#6733=VERTEX_POINT('',#22729);
#6734=VERTEX_POINT('',#22731);
#8077=EDGE_CURVE('',#6731,#6731,#5832,.T.);
#8078=EDGE_CURVE('',#6731,#6732,#4353,.T.);
#8079=EDGE_CURVE('',#6732,#6732,#5833,.T.);
#8080=EDGE_CURVE('',#6733,#6733,#5834,.T.);
#8081=EDGE_CURVE('',#6733,#6734,#4354,.T.);
#8082=EDGE_CURVE('',#6734,#6734,#5835,.T.);
#10675=ORIENTED_EDGE('',*,*,#8077,.F.);
#10676=ORIENTED_EDGE('',*,*,#8078,.T.);
#10677=ORIENTED_EDGE('',*,*,#8079,.T.);
#10678=ORIENTED_EDGE('',*,*,#8078,.F.);
#10679=ORIENTED_EDGE('',*,*,#8080,.F.);
#10680=ORIENTED_EDGE('',*,*,#8081,.T.);
#10681=ORIENTED_EDGE('',*,*,#8082,.T.);
#10682=ORIENTED_EDGE('',*,*,#8081,.F.);
#10683=ORIENTED_EDGE('',*,*,#8080,.T.);
#10684=ORIENTED_EDGE('',*,*,#8077,.T.);
#10685=ORIENTED_EDGE('',*,*,#8082,.F.);
#10686=ORIENTED_EDGE('',*,*,#8079,.F.);
#11559=CYLINDRICAL_SURFACE('',#15067,0.225);
#11560=CYLINDRICAL_SURFACE('',#15070,1.);
#12231=ADVANCED_FACE('',(#2506),#11559,.F.);
#12232=ADVANCED_FACE('',(#2507),#11560,.T.);
#12233=ADVANCED_FACE('',(#2508,#1426),#1792,.T.);
#12234=ADVANCED_FACE('',(#2509,#1427),#1793,.F.);
#12485=CLOSED_SHELL('',(#12231,#12232,#12233,#12234));
#15066=AXIS2_PLACEMENT_3D('',#22721,#18758,#18759);
#15067=AXIS2_PLACEMENT_3D('',#22722,#18760,#18761);
#15068=AXIS2_PLACEMENT_3D('',#22724,#18762,#18763);
#15069=AXIS2_PLACEMENT_3D('',#22727,#18765,#18766);
#15070=AXIS2_PLACEMENT_3D('',#22728,#18767,#18768);
#15071=AXIS2_PLACEMENT_3D('',#22730,#18769,#18770);
#15072=AXIS2_PLACEMENT_3D('',#22733,#18772,#18773);
#15073=AXIS2_PLACEMENT_3D('',#22734,#18774,#18775);
#15074=AXIS2_PLACEMENT_3D('',#22735,#18776,#18777);
#18758=DIRECTION('axis',(0.,0.,1.));
#18759=DIRECTION('refdir',(1.,0.,0.));
#18760=DIRECTION('center_axis',(0.,1.,0.));
#18761=DIRECTION('ref_axis',(1.,0.,0.));
#18762=DIRECTION('center_axis',(0.,-1.,0.));
#18763=DIRECTION('ref_axis',(1.,0.,0.));
#18764=DIRECTION('',(0.,-1.,0.));
#18765=DIRECTION('center_axis',(0.,-1.,0.));
#18766=DIRECTION('ref_axis',(1.,0.,0.));
#18767=DIRECTION('center_axis',(0.,1.,0.));
#18768=DIRECTION('ref_axis',(1.,0.,0.));
#18769=DIRECTION('center_axis',(0.,1.,0.));
#18770=DIRECTION('ref_axis',(1.,0.,0.));
#18771=DIRECTION('',(0.,-1.,0.));
#18772=DIRECTION('center_axis',(0.,1.,0.));
#18773=DIRECTION('ref_axis',(1.,0.,0.));
#18774=DIRECTION('center_axis',(0.,1.,0.));
#18775=DIRECTION('ref_axis',(1.,0.,0.));
#18776=DIRECTION('center_axis',(0.,1.,0.));
#18777=DIRECTION('ref_axis',(1.,0.,0.));
#22721=CARTESIAN_POINT('',(0.,0.,0.));
#22722=CARTESIAN_POINT('Origin',(9.39692620785909,-5.7,18.4202014332567));
#22723=CARTESIAN_POINT('',(9.17192620785909,-5.5,18.4202014332567));
#22724=CARTESIAN_POINT('Origin',(9.39692620785909,-5.5,18.4202014332567));
#22725=CARTESIAN_POINT('',(9.17192620785909,-5.7,18.4202014332567));
#22726=CARTESIAN_POINT('',(9.17192620785909,-5.7,18.4202014332567));
#22727=CARTESIAN_POINT('Origin',(9.39692620785909,-5.7,18.4202014332567));
#22728=CARTESIAN_POINT('Origin',(9.39692620785909,-5.7,18.4202014332567));
#22729=CARTESIAN_POINT('',(8.39692620785909,-5.5,18.4202014332567));
#22730=CARTESIAN_POINT('Origin',(9.39692620785909,-5.5,18.4202014332567));
#22731=CARTESIAN_POINT('',(8.39692620785909,-5.7,18.4202014332567));
#22732=CARTESIAN_POINT('',(8.39692620785909,-5.7,18.4202014332567));
#22733=CARTESIAN_POINT('Origin',(9.39692620785909,-5.7,18.4202014332567));
#22734=CARTESIAN_POINT('Origin',(9.39692620785909,-5.5,18.4202014332567));
#22735=CARTESIAN_POINT('Origin',(9.39692620785909,-5.7,18.4202014332567));
#23585=UNCERTAINTY_MEASURE_WITH_UNIT(LENGTH_MEASURE(0.001),#23729,
'DISTANCE_ACCURACY_VALUE',
'Maximum model space distance between geometric entities at asserted c
onnectivities');
#23611=UNCERTAINTY_MEASURE_WITH_UNIT(LENGTH_MEASURE(0.001),#23729,
'DISTANCE_ACCURACY_VALUE',
'Maximum model space distance between geometric entities at asserted c
onnectivities');
#23702=(
GEOMETRIC_REPRESENTATION_CONTEXT(3)
GLOBAL_UNCERTAINTY_ASSIGNED_CONTEXT((#23585))
GLOBAL_UNIT_ASSIGNED_CONTEXT((#23729,#23731,#23732))
REPRESENTATION_CONTEXT('','3D')
);
#23728=(
GEOMETRIC_REPRESENTATION_CONTEXT(3)
GLOBAL_UNCERTAINTY_ASSIGNED_CONTEXT((#23611))
GLOBAL_UNIT_ASSIGNED_CONTEXT((#23729,#23731,#23732))
REPRESENTATION_CONTEXT('','3D')
);
#23729=(
LENGTH_UNIT()
NAMED_UNIT(*)
SI_UNIT(.CENTI.,.METRE.)
);
#23731=(
NAMED_UNIT(*)
PLANE_ANGLE_UNIT()
SI_UNIT($,.RADIAN.)
);
#23732=(
NAMED_UNIT(*)
SI_UNIT($,.STERADIAN.)
SOLID_ANGLE_UNIT()
);
#23823=SHAPE_DEFINITION_REPRESENTATION(#23990,#24202);
#23990=PRODUCT_DEFINITION_SHAPE('',$,#24319);
#24202=SHAPE_REPRESENTATION('',(#15066),#23702);
#24228=PRODUCT_DEFINITION_CONTEXT('part definition',#24578,'design');
#24319=PRODUCT_DEFINITION('Pivot keeper (2)','Pivot keeper (2)',#24435,#24228);
#24435=PRODUCT_DEFINITION_FORMATION('',$,#24670);
#24578=APPLICATION_CONTEXT(
'Core Data for Automotive Mechanical Design Process');
#24579=PRODUCT_CONTEXT('part definition',#24578,'mechanical');
#24670=PRODUCT('Pivot keeper (2)','Pivot keeper (2)','Pivot keeper (2)',(#24579));
#24773=COLOUR_RGB('Off White',0.89,0.88,0.83);
#24774=FILL_AREA_STYLE_COLOUR('',#24773);
#24775=FILL_AREA_STYLE('',(#24774));
#24776=SURFACE_STYLE_FILL_AREA(#24775);
#24777=SURFACE_SIDE_STYLE('',(#24776));
#24778=SURFACE_STYLE_USAGE(.BOTH.,#24777);
#24779=PRESENTATION_STYLE_ASSIGNMENT((#24778));
ENDSEC;
END-ISO-10303-21;
